ISO-10303-21;
HEADER;
/* Generated by software containing ST-Developer
 * from STEP Tools, Inc. (www.steptools.com) 
 */

FILE_DESCRIPTION(
/* description */ ('Turntable on roller ring'),
/* implementation_level */ '2;1');

FILE_NAME(
/* name */ 'Inner race spacer (5).step',
/* time_stamp */ '2026-10-28T03:23:59-07:00',
/* author */ (''),
/* organization */ (''),
/* preprocessor_version */ 'ST-DEVELOPER v20.2',
/* originating_system */ 'Autodesk Translation Framework v15.17.0.0',
/* authorisation */ '');

FILE_SCHEMA (('AUTOMOTIVE_DESIGN { 1 0 10303 214 3 1 1 }'));
ENDSEC;

DATA;
#10=MECHANICAL_DESIGN_GEOMETRIC_PRESENTATION_REPRESENTATION('',(#655),#16281);
#536=SHAPE_REPRESENTATION_RELATIONSHIP('SRR','None',#16555,#591);
#591=ADVANCED_BREP_SHAPE_REPRESENTATION('',(#725),#16249);
#655=STYLED_ITEM('',(#16932),#725);
#725=MANIFOLD_SOLID_BREP('Body1',#8398);
#929=FACE_BOUND('',#2255,.T.);
#930=FACE_BOUND('',#2257,.T.);
#1157=PLANE('',#9752);
#1158=PLANE('',#9753);
#1575=FACE_OUTER_BOUND('',#2252,.T.);
#1576=FACE_OUTER_BOUND('',#2253,.T.);
#1577=FACE_OUTER_BOUND('',#2254,.T.);
#1578=FACE_OUTER_BOUND('',#2256,.T.);
#2252=EDGE_LOOP('',(#7007,#7008,#7009,#7010));
#2253=EDGE_LOOP('',(#7011,#7012,#7013,#7014));
#2254=EDGE_LOOP('',(#7015));
#2255=EDGE_LOOP('',(#7016));
#2256=EDGE_LOOP('',(#7017));
#2257=EDGE_LOOP('',(#7018));
#2835=LINE('',#14969,#3318);
#2836=LINE('',#14975,#3319);
#3318=VECTOR('',#11958,0.505);
#3319=VECTOR('',#11965,0.7);
#3777=CIRCLE('',#9747,0.505);
#3778=CIRCLE('',#9748,0.505);
#3779=CIRCLE('',#9750,0.7);
#3780=CIRCLE('',#9751,0.7);
#4405=VERTEX_POINT('',#14966);
#4406=VERTEX_POINT('',#14968);
#4407=VERTEX_POINT('',#14972);
#4408=VERTEX_POINT('',#14974);
#5314=EDGE_CURVE('',#4405,#4405,#3777,.T.);
#5315=EDGE_CURVE('',#4405,#4406,#2835,.T.);
#5316=EDGE_CURVE('',#4406,#4406,#3778,.T.);
#5317=EDGE_CURVE('',#4407,#4407,#3779,.T.);
#5318=EDGE_CURVE('',#4407,#4408,#2836,.T.);
#5319=EDGE_CURVE('',#4408,#4408,#3780,.T.);
#7007=ORIENTED_EDGE('',*,*,#5314,.F.);
#7008=ORIENTED_EDGE('',*,*,#5315,.T.);
#7009=ORIENTED_EDGE('',*,*,#5316,.T.);
#7010=ORIENTED_EDGE('',*,*,#5315,.F.);
#7011=ORIENTED_EDGE('',*,*,#5317,.F.);
#7012=ORIENTED_EDGE('',*,*,#5318,.T.);
#7013=ORIENTED_EDGE('',*,*,#5319,.T.);
#7014=ORIENTED_EDGE('',*,*,#5318,.F.);
#7015=ORIENTED_EDGE('',*,*,#5317,.T.);
#7016=ORIENTED_EDGE('',*,*,#5314,.T.);
#7017=ORIENTED_EDGE('',*,*,#5319,.F.);
#7018=ORIENTED_EDGE('',*,*,#5316,.F.);
#7794=CYLINDRICAL_SURFACE('',#9746,0.505);
#7795=CYLINDRICAL_SURFACE('',#9749,0.7);
#8178=ADVANCED_FACE('',(#1575),#7794,.F.);
#8179=ADVANCED_FACE('',(#1576),#7795,.T.);
#8180=ADVANCED_FACE('',(#1577,#929),#1157,.T.);
#8181=ADVANCED_FACE('',(#1578,#930),#1158,.F.);
#8398=CLOSED_SHELL('',(#8178,#8179,#8180,#8181));
#9745=AXIS2_PLACEMENT_3D('',#14964,#11952,#11953);
#9746=AXIS2_PLACEMENT_3D('',#14965,#11954,#11955);
#9747=AXIS2_PLACEMENT_3D('',#14967,#11956,#11957);
#9748=AXIS2_PLACEMENT_3D('',#14970,#11959,#11960);
#9749=AXIS2_PLACEMENT_3D('',#14971,#11961,#11962);
#9750=AXIS2_PLACEMENT_3D('',#14973,#11963,#11964);
#9751=AXIS2_PLACEMENT_3D('',#14976,#11966,#11967);
#9752=AXIS2_PLACEMENT_3D('',#14977,#11968,#11969);
#9753=AXIS2_PLACEMENT_3D('',#14978,#11970,#11971);
#11952=DIRECTION('axis',(0.,0.,1.));
#11953=DIRECTION('refdir',(1.,0.,0.));
#11954=DIRECTION('center_axis',(0.,1.,0.));
#11955=DIRECTION('ref_axis',(1.,0.,0.));
#11956=DIRECTION('center_axis',(0.,-1.,0.));
#11957=DIRECTION('ref_axis',(1.,0.,0.));
#11958=DIRECTION('',(0.,-1.,0.));
#11959=DIRECTION('center_axis',(0.,-1.,0.));
#11960=DIRECTION('ref_axis',(1.,0.,0.));
#11961=DIRECTION('center_axis',(0.,1.,0.));
#11962=DIRECTION('ref_axis',(1.,0.,0.));
#11963=DIRECTION('center_axis',(0.,1.,0.));
#11964=DIRECTION('ref_axis',(1.,0.,0.));
#11965=DIRECTION('',(0.,-1.,0.));
#11966=DIRECTION('center_axis',(0.,1.,0.));
#11967=DIRECTION('ref_axis',(1.,0.,0.));
#11968=DIRECTION('center_axis',(0.,1.,0.));
#11969=DIRECTION('ref_axis',(1.,0.,0.));
#11970=DIRECTION('center_axis',(0.,1.,0.));
#11971=DIRECTION('ref_axis',(1.,0.,0.));
#14964=CARTESIAN_POINT('',(0.,0.,0.));
#14965=CARTESIAN_POINT('Origin',(0.,15.45,3.5));
#14966=CARTESIAN_POINT('',(-0.505,15.9,3.5));
#14967=CARTESIAN_POINT('Origin',(0.,15.9,3.5));
#14968=CARTESIAN_POINT('',(-0.505,15.45,3.5));
#14969=CARTESIAN_POINT('',(-0.505,15.45,3.5));
#14970=CARTESIAN_POINT('Origin',(0.,15.45,3.5));
#14971=CARTESIAN_POINT('Origin',(0.,15.45,3.5));
#14972=CARTESIAN_POINT('',(-0.7,15.9,3.5));
#14973=CARTESIAN_POINT('Origin',(0.,15.9,3.5));
#14974=CARTESIAN_POINT('',(-0.7,15.45,3.5));
#14975=CARTESIAN_POINT('',(-0.7,15.45,3.5));
#14976=CARTESIAN_POINT('Origin',(0.,15.45,3.5));
#14977=CARTESIAN_POINT('Origin',(0.,15.9,3.5));
#14978=CARTESIAN_POINT('Origin',(0.,15.45,3.5));
#16180=UNCERTAINTY_MEASURE_WITH_UNIT(LENGTH_MEASURE(0.001),#16282,
'DISTANCE_ACCURACY_VALUE',
'Maximum model space distance between geometric entities at asserted c
onnectivities');
#16212=UNCERTAINTY_MEASURE_WITH_UNIT(LENGTH_MEASURE(0.001),#16282,
'DISTANCE_ACCURACY_VALUE',
'Maximum model space distance between geometric entities at asserted c
onnectivities');
#16249=(
GEOMETRIC_REPRESENTATION_CONTEXT(3)
GLOBAL_UNCERTAINTY_ASSIGNED_CONTEXT((#16180))
GLOBAL_UNIT_ASSIGNED_CONTEXT((#16282,#16284,#16285))
REPRESENTATION_CONTEXT('','3D')
);
#16281=(
GEOMETRIC_REPRESENTATION_CONTEXT(3)
GLOBAL_UNCERTAINTY_ASSIGNED_CONTEXT((#16212))
GLOBAL_UNIT_ASSIGNED_CONTEXT((#16282,#16284,#16285))
REPRESENTATION_CONTEXT('','3D')
);
#16282=(
LENGTH_UNIT()
NAMED_UNIT(*)
SI_UNIT(.CENTI.,.METRE.)
);
#16284=(
NAMED_UNIT(*)
PLANE_ANGLE_UNIT()
SI_UNIT($,.RADIAN.)
);
#16285=(
NAMED_UNIT(*)
SI_UNIT($,.STERADIAN.)
SOLID_ANGLE_UNIT()
);
#16322=SHAPE_DEFINITION_REPRESENTATION(#16416,#16555);
#16416=PRODUCT_DEFINITION_SHAPE('',$,#16624);
#16555=SHAPE_REPRESENTATION('',(#9745),#16249);
#16587=PRODUCT_DEFINITION_CONTEXT('part definition',#16793,'design');
#16624=PRODUCT_DEFINITION('Inner race spacer (5)','Inner race spacer (5)',
#16692,#16587);
#16692=PRODUCT_DEFINITION_FORMATION('',$,#16831);
#16793=APPLICATION_CONTEXT(
'Core Data for Automotive Mechanical Design Process');
#16794=PRODUCT_CONTEXT('part definition',#16793,'mechanical');
#16831=PRODUCT('Inner race spacer (5)','Inner race spacer (5)',
'Inner race spacer (5)',(#16794));
#16926=COLOUR_RGB('Grey',0.48,0.52,0.57);
#16927=FILL_AREA_STYLE_COLOUR('',#16926);
#16928=FILL_AREA_STYLE('',(#16927));
#16929=SURFACE_STYLE_FILL_AREA(#16928);
#16930=SURFACE_SIDE_STYLE('',(#16929));
#16931=SURFACE_STYLE_USAGE(.BOTH.,#16930);
#16932=PRESENTATION_STYLE_ASSIGNMENT((#16931));
ENDSEC;
END-ISO-10303-21;
